ISO-10303-21;
HEADER;
/* Generated by software containing ST-Developer
 * from STEP Tools, Inc. (www.steptools.com) 
 */

FILE_DESCRIPTION(
/* description */ ('PAT-054'),
/* implementation_level */ '2;1');

FILE_NAME(
/* name */ 'Flat Washer - M6.step',
/* time_stamp */ '2026-10-29T16:38:13-07:00',
/* author */ (''),
/* organization */ (''),
/* preprocessor_version */ 'ST-DEVELOPER v20.2',
/* originating_system */ 'Autodesk Translation Framework v15.17.0.0',
/* authorisation */ '');

FILE_SCHEMA (('AUTOMOTIVE_DESIGN { 1 0 10303 214 3 1 1 }'));
ENDSEC;

DATA;
#10=MECHANICAL_DESIGN_GEOMETRIC_PRESENTATION_REPRESENTATION('',(#956),#33981);
#853=SHAPE_REPRESENTATION_RELATIONSHIP('SRR','None',#34231,#897);
#897=ADVANCED_BREP_SHAPE_REPRESENTATION('',(#1011),#33979);
#956=STYLED_ITEM('',(#34524),#1011);
#1011=MANIFOLD_SOLID_BREP('Body1',#13071);
#1225=FACE_BOUND('',#3216,.T.);
#1226=FACE_BOUND('',#3218,.T.);
#1562=PLANE('',#14801);
#1563=PLANE('',#14802);
#2277=FACE_OUTER_BOUND('',#3213,.T.);
#2278=FACE_OUTER_BOUND('',#3214,.T.);
#2279=FACE_OUTER_BOUND('',#3215,.T.);
#2280=FACE_OUTER_BOUND('',#3217,.T.);
#3213=EDGE_LOOP('',(#11903,#11904,#11905,#11906));
#3214=EDGE_LOOP('',(#11907,#11908,#11909,#11910));
#3215=EDGE_LOOP('',(#11911));
#3216=EDGE_LOOP('',(#11912));
#3217=EDGE_LOOP('',(#11913));
#3218=EDGE_LOOP('',(#11914));
#4145=LINE('',#33737,#5079);
#4146=LINE('',#33743,#5080);
#5079=VECTOR('',#18274,0.32);
#5080=VECTOR('',#18281,0.6);
#5558=CIRCLE('',#14796,0.32);
#5559=CIRCLE('',#14797,0.32);
#5560=CIRCLE('',#14799,0.6);
#5561=CIRCLE('',#14800,0.6);
#6720=VERTEX_POINT('',#33734);
#6721=VERTEX_POINT('',#33736);
#6722=VERTEX_POINT('',#33740);
#6723=VERTEX_POINT('',#33742);
#8451=EDGE_CURVE('',#6720,#6720,#5558,.T.);
#8452=EDGE_CURVE('',#6720,#6721,#4145,.T.);
#8453=EDGE_CURVE('',#6721,#6721,#5559,.T.);
#8454=EDGE_CURVE('',#6722,#6722,#5560,.T.);
#8455=EDGE_CURVE('',#6722,#6723,#4146,.T.);
#8456=EDGE_CURVE('',#6723,#6723,#5561,.T.);
#11903=ORIENTED_EDGE('',*,*,#8451,.F.);
#11904=ORIENTED_EDGE('',*,*,#8452,.T.);
#11905=ORIENTED_EDGE('',*,*,#8453,.T.);
#11906=ORIENTED_EDGE('',*,*,#8452,.F.);
#11907=ORIENTED_EDGE('',*,*,#8454,.F.);
#11908=ORIENTED_EDGE('',*,*,#8455,.T.);
#11909=ORIENTED_EDGE('',*,*,#8456,.T.);
#11910=ORIENTED_EDGE('',*,*,#8455,.F.);
#11911=ORIENTED_EDGE('',*,*,#8454,.T.);
#11912=ORIENTED_EDGE('',*,*,#8451,.T.);
#11913=ORIENTED_EDGE('',*,*,#8456,.F.);
#11914=ORIENTED_EDGE('',*,*,#8453,.F.);
#12283=CYLINDRICAL_SURFACE('',#14795,0.32);
#12284=CYLINDRICAL_SURFACE('',#14798,0.6);
#12989=ADVANCED_FACE('',(#2277),#12283,.F.);
#12990=ADVANCED_FACE('',(#2278),#12284,.T.);
#12991=ADVANCED_FACE('',(#2279,#1225),#1562,.T.);
#12992=ADVANCED_FACE('',(#2280,#1226),#1563,.F.);
#13071=CLOSED_SHELL('',(#12989,#12990,#12991,#12992));
#14794=AXIS2_PLACEMENT_3D('',#33732,#18268,#18269);
#14795=AXIS2_PLACEMENT_3D('',#33733,#18270,#18271);
#14796=AXIS2_PLACEMENT_3D('',#33735,#18272,#18273);
#14797=AXIS2_PLACEMENT_3D('',#33738,#18275,#18276);
#14798=AXIS2_PLACEMENT_3D('',#33739,#18277,#18278);
#14799=AXIS2_PLACEMENT_3D('',#33741,#18279,#18280);
#14800=AXIS2_PLACEMENT_3D('',#33744,#18282,#18283);
#14801=AXIS2_PLACEMENT_3D('',#33745,#18284,#18285);
#14802=AXIS2_PLACEMENT_3D('',#33746,#18286,#18287);
#18268=DIRECTION('axis',(0.,0.,1.));
#18269=DIRECTION('refdir',(1.,0.,0.));
#18270=DIRECTION('center_axis',(0.,1.,0.));
#18271=DIRECTION('ref_axis',(1.,0.,0.));
#18272=DIRECTION('center_axis',(0.,-1.,0.));
#18273=DIRECTION('ref_axis',(1.,0.,0.));
#18274=DIRECTION('',(0.,-1.,0.));
#18275=DIRECTION('center_axis',(0.,-1.,0.));
#18276=DIRECTION('ref_axis',(1.,0.,0.));
#18277=DIRECTION('center_axis',(0.,1.,0.));
#18278=DIRECTION('ref_axis',(1.,0.,0.));
#18279=DIRECTION('center_axis',(0.,1.,0.));
#18280=DIRECTION('ref_axis',(1.,0.,0.));
#18281=DIRECTION('',(0.,-1.,0.));
#18282=DIRECTION('center_axis',(0.,1.,0.));
#18283=DIRECTION('ref_axis',(1.,0.,0.));
#18284=DIRECTION('center_axis',(0.,1.,0.));
#18285=DIRECTION('ref_axis',(1.,0.,0.));
#18286=DIRECTION('center_axis',(0.,1.,0.));
#18287=DIRECTION('ref_axis',(1.,0.,0.));
#33732=CARTESIAN_POINT('',(0.,0.,0.));
#33733=CARTESIAN_POINT('Origin',(0.,0.,0.));
#33734=CARTESIAN_POINT('',(-0.32,0.16,3.91886975727153E-17));
#33735=CARTESIAN_POINT('Origin',(0.,0.16,0.));
#33736=CARTESIAN_POINT('',(-0.32,0.,3.91886975727153E-17));
#33737=CARTESIAN_POINT('',(-0.32,0.,3.91886975727153E-17));
#33738=CARTESIAN_POINT('Origin',(0.,0.,0.));
#33739=CARTESIAN_POINT('Origin',(0.,0.,0.));
#33740=CARTESIAN_POINT('',(-0.6,0.16,7.34788079488412E-17));
#33741=CARTESIAN_POINT('Origin',(0.,0.16,0.));
#33742=CARTESIAN_POINT('',(-0.6,0.,7.34788079488412E-17));
#33743=CARTESIAN_POINT('',(-0.6,0.,7.34788079488412E-17));
#33744=CARTESIAN_POINT('Origin',(0.,0.,0.));
#33745=CARTESIAN_POINT('Origin',(0.,0.16,0.));
#33746=CARTESIAN_POINT('Origin',(0.,0.,0.));
#33927=UNCERTAINTY_MEASURE_WITH_UNIT(LENGTH_MEASURE(0.001),#33982,
'DISTANCE_ACCURACY_VALUE',
'Maximum model space distance between geometric entities at asserted c
onnectivities');
#33929=UNCERTAINTY_MEASURE_WITH_UNIT(LENGTH_MEASURE(0.001),#33982,
'DISTANCE_ACCURACY_VALUE',
'Maximum model space distance between geometric entities at asserted c
onnectivities');
#33979=(
GEOMETRIC_REPRESENTATION_CONTEXT(3)
GLOBAL_UNCERTAINTY_ASSIGNED_CONTEXT((#33927))
GLOBAL_UNIT_ASSIGNED_CONTEXT((#33982,#33984,#33985))
REPRESENTATION_CONTEXT('','3D')
);
#33981=(
GEOMETRIC_REPRESENTATION_CONTEXT(3)
GLOBAL_UNCERTAINTY_ASSIGNED_CONTEXT((#33929))
GLOBAL_UNIT_ASSIGNED_CONTEXT((#33982,#33984,#33985))
REPRESENTATION_CONTEXT('','3D')
);
#33982=(
LENGTH_UNIT()
NAMED_UNIT(*)
SI_UNIT(.CENTI.,.METRE.)
);
#33984=(
NAMED_UNIT(*)
PLANE_ANGLE_UNIT()
SI_UNIT($,.RADIAN.)
);
#33985=(
NAMED_UNIT(*)
SI_UNIT($,.STERADIAN.)
SOLID_ANGLE_UNIT()
);
#34035=SHAPE_DEFINITION_REPRESENTATION(#34119,#34231);
#34119=PRODUCT_DEFINITION_SHAPE('',$,#34283);
#34231=SHAPE_REPRESENTATION('',(#14794),#33979);
#34233=PRODUCT_DEFINITION_CONTEXT('part definition',#34388,'design');
#34283=PRODUCT_DEFINITION('Flat Washer - M6','Flat Washer - M6',#34334,
#34233);
#34334=PRODUCT_DEFINITION_FORMATION('',$,#34439);
#34388=APPLICATION_CONTEXT(
'Core Data for Automotive Mechanical Design Process');
#34389=PRODUCT_CONTEXT('part definition',#34388,'mechanical');
#34439=PRODUCT('Flat Washer - M6','Flat Washer - M6','Flat Washer - M6',
(#34389));
#34518=COLOUR_RGB('Black',0.12,0.14,0.17);
#34519=FILL_AREA_STYLE_COLOUR('',#34518);
#34520=FILL_AREA_STYLE('',(#34519));
#34521=SURFACE_STYLE_FILL_AREA(#34520);
#34522=SURFACE_SIDE_STYLE('',(#34521));
#34523=SURFACE_STYLE_USAGE(.BOTH.,#34522);
#34524=PRESENTATION_STYLE_ASSIGNMENT((#34523));
ENDSEC;
END-ISO-10303-21;
